ISO-10303-21;
HEADER;
/* Generated by software containing ST-Developer
 * from STEP Tools, Inc. (www.steptools.com) 
 */

FILE_DESCRIPTION(
/* description */ ('Double-row support with tensioned shaft'),
/* implementation_level */ '2;1');

FILE_NAME(
/* name */ 'Adjustment nut.step',
/* time_stamp */ '2026-10-27T10:50:35-07:00',
/* author */ (''),
/* organization */ (''),
/* preprocessor_version */ 'ST-DEVELOPER v20.2',
/* originating_system */ 'Autodesk Translation Framework v15.17.0.0',
/* authorisation */ '');

FILE_SCHEMA (('AUTOMOTIVE_DESIGN { 1 0 10303 214 3 1 1 }'));
ENDSEC;

DATA;
#10=MECHANICAL_DESIGN_GEOMETRIC_PRESENTATION_REPRESENTATION('',(#507),#11559);
#442=SHAPE_REPRESENTATION_RELATIONSHIP('SRR','None',#11752,#474);
#474=ADVANCED_BREP_SHAPE_REPRESENTATION('',(#537),#11554);
#507=STYLED_ITEM('',(#11974),#537);
#537=MANIFOLD_SOLID_BREP('Body1',#6355);
#660=FACE_BOUND('',#1673,.T.);
#661=FACE_BOUND('',#1675,.T.);
#873=PLANE('',#7275);
#874=PLANE('',#7276);
#875=PLANE('',#7277);
#876=PLANE('',#7278);
#877=PLANE('',#7279);
#878=PLANE('',#7280);
#879=PLANE('',#7281);
#880=PLANE('',#7282);
#1203=FACE_OUTER_BOUND('',#1665,.T.);
#1204=FACE_OUTER_BOUND('',#1666,.T.);
#1205=FACE_OUTER_BOUND('',#1667,.T.);
#1206=FACE_OUTER_BOUND('',#1668,.T.);
#1207=FACE_OUTER_BOUND('',#1669,.T.);
#1208=FACE_OUTER_BOUND('',#1670,.T.);
#1209=FACE_OUTER_BOUND('',#1671,.T.);
#1210=FACE_OUTER_BOUND('',#1672,.T.);
#1211=FACE_OUTER_BOUND('',#1674,.T.);
#1665=EDGE_LOOP('',(#5622,#5623,#5624,#5625));
#1666=EDGE_LOOP('',(#5626,#5627,#5628,#5629));
#1667=EDGE_LOOP('',(#5630,#5631,#5632,#5633));
#1668=EDGE_LOOP('',(#5634,#5635,#5636,#5637));
#1669=EDGE_LOOP('',(#5638,#5639,#5640,#5641));
#1670=EDGE_LOOP('',(#5642,#5643,#5644,#5645));
#1671=EDGE_LOOP('',(#5646,#5647,#5648,#5649));
#1672=EDGE_LOOP('',(#5650,#5651,#5652,#5653,#5654,#5655));
#1673=EDGE_LOOP('',(#5656));
#1674=EDGE_LOOP('',(#5657,#5658,#5659,#5660,#5661,#5662));
#1675=EDGE_LOOP('',(#5663));
#2186=LINE('',#11143,#2733);
#2187=LINE('',#11148,#2734);
#2188=LINE('',#11150,#2735);
#2189=LINE('',#11152,#2736);
#2190=LINE('',#11153,#2737);
#2191=LINE('',#11156,#2738);
#2192=LINE('',#11158,#2739);
#2193=LINE('',#11159,#2740);
#2194=LINE('',#11162,#2741);
#2195=LINE('',#11164,#2742);
#2196=LINE('',#11165,#2743);
#2197=LINE('',#11168,#2744);
#2198=LINE('',#11170,#2745);
#2199=LINE('',#11171,#2746);
#2200=LINE('',#11174,#2747);
#2201=LINE('',#11176,#2748);
#2202=LINE('',#11177,#2749);
#2203=LINE('',#11179,#2750);
#2204=LINE('',#11180,#2751);
#2733=VECTOR('',#8937,0.54);
#2734=VECTOR('',#8942,1.);
#2735=VECTOR('',#8943,1.);
#2736=VECTOR('',#8944,1.);
#2737=VECTOR('',#8945,1.);
#2738=VECTOR('',#8948,1.);
#2739=VECTOR('',#8949,1.);
#2740=VECTOR('',#8950,1.);
#2741=VECTOR('',#8953,1.);
#2742=VECTOR('',#8954,1.);
#2743=VECTOR('',#8955,1.);
#2744=VECTOR('',#8958,1.);
#2745=VECTOR('',#8959,1.);
#2746=VECTOR('',#8960,1.);
#2747=VECTOR('',#8963,1.);
#2748=VECTOR('',#8964,1.);
#2749=VECTOR('',#8965,1.);
#2750=VECTOR('',#8968,1.);
#2751=VECTOR('',#8969,1.);
#3000=CIRCLE('',#7273,0.54);
#3001=CIRCLE('',#7274,0.54);
#3461=VERTEX_POINT('',#11140);
#3462=VERTEX_POINT('',#11142);
#3463=VERTEX_POINT('',#11146);
#3464=VERTEX_POINT('',#11147);
#3465=VERTEX_POINT('',#11149);
#3466=VERTEX_POINT('',#11151);
#3467=VERTEX_POINT('',#11155);
#3468=VERTEX_POINT('',#11157);
#3469=VERTEX_POINT('',#11161);
#3470=VERTEX_POINT('',#11163);
#3471=VERTEX_POINT('',#11167);
#3472=VERTEX_POINT('',#11169);
#3473=VERTEX_POINT('',#11173);
#3474=VERTEX_POINT('',#11175);
#4196=EDGE_CURVE('',#3461,#3461,#3000,.T.);
#4197=EDGE_CURVE('',#3461,#3462,#2186,.T.);
#4198=EDGE_CURVE('',#3462,#3462,#3001,.T.);
#4199=EDGE_CURVE('',#3463,#3464,#2187,.T.);
#4200=EDGE_CURVE('',#3463,#3465,#2188,.T.);
#4201=EDGE_CURVE('',#3466,#3465,#2189,.T.);
#4202=EDGE_CURVE('',#3464,#3466,#2190,.T.);
#4203=EDGE_CURVE('',#3464,#3467,#2191,.T.);
#4204=EDGE_CURVE('',#3468,#3466,#2192,.T.);
#4205=EDGE_CURVE('',#3467,#3468,#2193,.T.);
#4206=EDGE_CURVE('',#3467,#3469,#2194,.T.);
#4207=EDGE_CURVE('',#3470,#3468,#2195,.T.);
#4208=EDGE_CURVE('',#3469,#3470,#2196,.T.);
#4209=EDGE_CURVE('',#3469,#3471,#2197,.T.);
#4210=EDGE_CURVE('',#3472,#3470,#2198,.T.);
#4211=EDGE_CURVE('',#3471,#3472,#2199,.T.);
#4212=EDGE_CURVE('',#3471,#3473,#2200,.T.);
#4213=EDGE_CURVE('',#3474,#3472,#2201,.T.);
#4214=EDGE_CURVE('',#3473,#3474,#2202,.T.);
#4215=EDGE_CURVE('',#3473,#3463,#2203,.T.);
#4216=EDGE_CURVE('',#3465,#3474,#2204,.T.);
#5622=ORIENTED_EDGE('',*,*,#4196,.F.);
#5623=ORIENTED_EDGE('',*,*,#4197,.T.);
#5624=ORIENTED_EDGE('',*,*,#4198,.F.);
#5625=ORIENTED_EDGE('',*,*,#4197,.F.);
#5626=ORIENTED_EDGE('',*,*,#4199,.F.);
#5627=ORIENTED_EDGE('',*,*,#4200,.T.);
#5628=ORIENTED_EDGE('',*,*,#4201,.F.);
#5629=ORIENTED_EDGE('',*,*,#4202,.F.);
#5630=ORIENTED_EDGE('',*,*,#4203,.F.);
#5631=ORIENTED_EDGE('',*,*,#4202,.T.);
#5632=ORIENTED_EDGE('',*,*,#4204,.F.);
#5633=ORIENTED_EDGE('',*,*,#4205,.F.);
#5634=ORIENTED_EDGE('',*,*,#4206,.F.);
#5635=ORIENTED_EDGE('',*,*,#4205,.T.);
#5636=ORIENTED_EDGE('',*,*,#4207,.F.);
#5637=ORIENTED_EDGE('',*,*,#4208,.F.);
#5638=ORIENTED_EDGE('',*,*,#4209,.F.);
#5639=ORIENTED_EDGE('',*,*,#4208,.T.);
#5640=ORIENTED_EDGE('',*,*,#4210,.F.);
#5641=ORIENTED_EDGE('',*,*,#4211,.F.);
#5642=ORIENTED_EDGE('',*,*,#4212,.F.);
#5643=ORIENTED_EDGE('',*,*,#4211,.T.);
#5644=ORIENTED_EDGE('',*,*,#4213,.F.);
#5645=ORIENTED_EDGE('',*,*,#4214,.F.);
#5646=ORIENTED_EDGE('',*,*,#4215,.F.);
#5647=ORIENTED_EDGE('',*,*,#4214,.T.);
#5648=ORIENTED_EDGE('',*,*,#4216,.F.);
#5649=ORIENTED_EDGE('',*,*,#4200,.F.);
#5650=ORIENTED_EDGE('',*,*,#4216,.T.);
#5651=ORIENTED_EDGE('',*,*,#4213,.T.);
#5652=ORIENTED_EDGE('',*,*,#4210,.T.);
#5653=ORIENTED_EDGE('',*,*,#4207,.T.);
#5654=ORIENTED_EDGE('',*,*,#4204,.T.);
#5655=ORIENTED_EDGE('',*,*,#4201,.T.);
#5656=ORIENTED_EDGE('',*,*,#4198,.T.);
#5657=ORIENTED_EDGE('',*,*,#4215,.T.);
#5658=ORIENTED_EDGE('',*,*,#4199,.T.);
#5659=ORIENTED_EDGE('',*,*,#4203,.T.);
#5660=ORIENTED_EDGE('',*,*,#4206,.T.);
#5661=ORIENTED_EDGE('',*,*,#4209,.T.);
#5662=ORIENTED_EDGE('',*,*,#4212,.T.);
#5663=ORIENTED_EDGE('',*,*,#4196,.T.);
#5968=CYLINDRICAL_SURFACE('',#7272,0.54);
#6266=ADVANCED_FACE('',(#1203),#5968,.F.);
#6267=ADVANCED_FACE('',(#1204),#873,.T.);
#6268=ADVANCED_FACE('',(#1205),#874,.T.);
#6269=ADVANCED_FACE('',(#1206),#875,.T.);
#6270=ADVANCED_FACE('',(#1207),#876,.T.);
#6271=ADVANCED_FACE('',(#1208),#877,.T.);
#6272=ADVANCED_FACE('',(#1209),#878,.T.);
#6273=ADVANCED_FACE('',(#1210,#660),#879,.T.);
#6274=ADVANCED_FACE('',(#1211,#661),#880,.F.);
#6355=CLOSED_SHELL('',(#6266,#6267,#6268,#6269,#6270,#6271,#6272,#6273,
#6274));
#7271=AXIS2_PLACEMENT_3D('',#11138,#8931,#8932);
#7272=AXIS2_PLACEMENT_3D('',#11139,#8933,#8934);
#7273=AXIS2_PLACEMENT_3D('',#11141,#8935,#8936);
#7274=AXIS2_PLACEMENT_3D('',#11144,#8938,#8939);
#7275=AXIS2_PLACEMENT_3D('',#11145,#8940,#8941);
#7276=AXIS2_PLACEMENT_3D('',#11154,#8946,#8947);
#7277=AXIS2_PLACEMENT_3D('',#11160,#8951,#8952);
#7278=AXIS2_PLACEMENT_3D('',#11166,#8956,#8957);
#7279=AXIS2_PLACEMENT_3D('',#11172,#8961,#8962);
#7280=AXIS2_PLACEMENT_3D('',#11178,#8966,#8967);
#7281=AXIS2_PLACEMENT_3D('',#11181,#8970,#8971);
#7282=AXIS2_PLACEMENT_3D('',#11182,#8972,#8973);
#8931=DIRECTION('axis',(0.,0.,1.));
#8932=DIRECTION('refdir',(1.,0.,0.));
#8933=DIRECTION('center_axis',(0.,1.,0.));
#8934=DIRECTION('ref_axis',(1.,0.,0.));
#8935=DIRECTION('center_axis',(0.,1.,0.));
#8936=DIRECTION('ref_axis',(1.,0.,0.));
#8937=DIRECTION('',(0.,1.,0.));
#8938=DIRECTION('center_axis',(0.,-1.,0.));
#8939=DIRECTION('ref_axis',(1.,0.,0.));
#8940=DIRECTION('center_axis',(0.866025403784439,0.,-0.5));
#8941=DIRECTION('ref_axis',(-0.5,0.,-0.866025403784439));
#8942=DIRECTION('',(0.5,0.,0.866025403784438));
#8943=DIRECTION('',(0.,1.,0.));
#8944=DIRECTION('',(-0.5,0.,-0.866025403784438));
#8945=DIRECTION('',(0.,1.,0.));
#8946=DIRECTION('center_axis',(0.866025403784439,0.,0.5));
#8947=DIRECTION('ref_axis',(0.5,0.,-0.866025403784439));
#8948=DIRECTION('',(-0.5,0.,0.866025403784438));
#8949=DIRECTION('',(0.5,0.,-0.866025403784438));
#8950=DIRECTION('',(0.,1.,0.));
#8951=DIRECTION('center_axis',(0.,0.,1.));
#8952=DIRECTION('ref_axis',(1.,0.,0.));
#8953=DIRECTION('',(-1.,0.,0.));
#8954=DIRECTION('',(1.,0.,0.));
#8955=DIRECTION('',(0.,1.,0.));
#8956=DIRECTION('center_axis',(-0.866025403784438,0.,0.5));
#8957=DIRECTION('ref_axis',(0.5,0.,0.866025403784438));
#8958=DIRECTION('',(-0.5,0.,-0.866025403784438));
#8959=DIRECTION('',(0.5,0.,0.866025403784438));
#8960=DIRECTION('',(0.,1.,0.));
#8961=DIRECTION('center_axis',(-0.866025403784439,0.,-0.5));
#8962=DIRECTION('ref_axis',(-0.5,0.,0.866025403784439));
#8963=DIRECTION('',(0.5,0.,-0.866025403784439));
#8964=DIRECTION('',(-0.5,0.,0.866025403784439));
#8965=DIRECTION('',(0.,1.,0.));
#8966=DIRECTION('center_axis',(0.,0.,-1.));
#8967=DIRECTION('ref_axis',(-1.,0.,0.));
#8968=DIRECTION('',(1.,0.,0.));
#8969=DIRECTION('',(-1.,0.,0.));
#8970=DIRECTION('center_axis',(0.,1.,0.));
#8971=DIRECTION('ref_axis',(0.,0.,1.));
#8972=DIRECTION('center_axis',(0.,1.,0.));
#8973=DIRECTION('ref_axis',(1.,0.,0.));
#11138=CARTESIAN_POINT('',(0.,0.,0.));
#11139=CARTESIAN_POINT('Origin',(0.,20.9,10.));
#11140=CARTESIAN_POINT('',(-0.54,21.,10.));
#11141=CARTESIAN_POINT('Origin',(0.,21.,10.));
#11142=CARTESIAN_POINT('',(-0.54,21.8,10.));
#11143=CARTESIAN_POINT('',(-0.54,20.9,10.));
#11144=CARTESIAN_POINT('Origin',(0.,21.8,10.));
#11145=CARTESIAN_POINT('Origin',(1.09696551146029,21.,10.));
#11146=CARTESIAN_POINT('',(0.548482755730145,21.,9.05));
#11147=CARTESIAN_POINT('',(1.09696551146029,21.,10.));
#11148=CARTESIAN_POINT('',(0.548482755730145,21.,9.05));
#11149=CARTESIAN_POINT('',(0.548482755730145,21.8,9.05));
#11150=CARTESIAN_POINT('',(0.548482755730145,21.,9.05));
#11151=CARTESIAN_POINT('',(1.09696551146029,21.8,10.));
#11152=CARTESIAN_POINT('',(0.548482755730145,21.8,9.05));
#11153=CARTESIAN_POINT('',(1.09696551146029,21.,10.));
#11154=CARTESIAN_POINT('Origin',(0.548482755730145,21.,10.95));
#11155=CARTESIAN_POINT('',(0.548482755730145,21.,10.95));
#11156=CARTESIAN_POINT('',(1.09696551146029,21.,10.));
#11157=CARTESIAN_POINT('',(0.548482755730145,21.8,10.95));
#11158=CARTESIAN_POINT('',(1.09696551146029,21.8,10.));
#11159=CARTESIAN_POINT('',(0.548482755730145,21.,10.95));
#11160=CARTESIAN_POINT('Origin',(-0.548482755730144,21.,10.95));
#11161=CARTESIAN_POINT('',(-0.548482755730144,21.,10.95));
#11162=CARTESIAN_POINT('',(0.548482755730145,21.,10.95));
#11163=CARTESIAN_POINT('',(-0.548482755730144,21.8,10.95));
#11164=CARTESIAN_POINT('',(0.548482755730145,21.8,10.95));
#11165=CARTESIAN_POINT('',(-0.548482755730144,21.,10.95));
#11166=CARTESIAN_POINT('Origin',(-1.09696551146029,21.,10.));
#11167=CARTESIAN_POINT('',(-1.09696551146029,21.,10.));
#11168=CARTESIAN_POINT('',(-0.548482755730144,21.,10.95));
#11169=CARTESIAN_POINT('',(-1.09696551146029,21.8,10.));
#11170=CARTESIAN_POINT('',(-0.548482755730144,21.8,10.95));
#11171=CARTESIAN_POINT('',(-1.09696551146029,21.,10.));
#11172=CARTESIAN_POINT('Origin',(-0.548482755730145,21.,9.05));
#11173=CARTESIAN_POINT('',(-0.548482755730145,21.,9.05));
#11174=CARTESIAN_POINT('',(-1.09696551146029,21.,10.));
#11175=CARTESIAN_POINT('',(-0.548482755730145,21.8,9.05));
#11176=CARTESIAN_POINT('',(-1.09696551146029,21.8,10.));
#11177=CARTESIAN_POINT('',(-0.548482755730145,21.,9.05));
#11178=CARTESIAN_POINT('Origin',(0.548482755730145,21.,9.05));
#11179=CARTESIAN_POINT('',(-0.548482755730145,21.,9.05));
#11180=CARTESIAN_POINT('',(-0.548482755730145,21.8,9.05));
#11181=CARTESIAN_POINT('Origin',(0.,21.8,10.));
#11182=CARTESIAN_POINT('Origin',(0.,21.,10.));
#11517=UNCERTAINTY_MEASURE_WITH_UNIT(LENGTH_MEASURE(0.001),#11560,
'DISTANCE_ACCURACY_VALUE',
'Maximum model space distance between geometric entities at asserted c
onnectivities');
#11522=UNCERTAINTY_MEASURE_WITH_UNIT(LENGTH_MEASURE(0.001),#11560,
'DISTANCE_ACCURACY_VALUE',
'Maximum model space distance between geometric entities at asserted c
onnectivities');
#11554=(
GEOMETRIC_REPRESENTATION_CONTEXT(3)
GLOBAL_UNCERTAINTY_ASSIGNED_CONTEXT((#11517))
GLOBAL_UNIT_ASSIGNED_CONTEXT((#11560,#11562,#11563))
REPRESENTATION_CONTEXT('','3D')
);
#11559=(
GEOMETRIC_REPRESENTATION_CONTEXT(3)
GLOBAL_UNCERTAINTY_ASSIGNED_CONTEXT((#11522))
GLOBAL_UNIT_ASSIGNED_CONTEXT((#11560,#11562,#11563))
REPRESENTATION_CONTEXT('','3D')
);
#11560=(
LENGTH_UNIT()
NAMED_UNIT(*)
SI_UNIT(.CENTI.,.METRE.)
);
#11562=(
NAMED_UNIT(*)
PLANE_ANGLE_UNIT()
SI_UNIT($,.RADIAN.)
);
#11563=(
NAMED_UNIT(*)
SI_UNIT($,.STERADIAN.)
SOLID_ANGLE_UNIT()
);
#11595=SHAPE_DEFINITION_REPRESENTATION(#11706,#11752);
#11706=PRODUCT_DEFINITION_SHAPE('',$,#11789);
#11752=SHAPE_REPRESENTATION('',(#7271),#11554);
#11757=PRODUCT_DEFINITION_CONTEXT('part definition',#11867,'design');
#11789=PRODUCT_DEFINITION('Adjustment nut','Adjustment nut',#11825,#11757);
#11825=PRODUCT_DEFINITION_FORMATION('',$,#11900);
#11867=APPLICATION_CONTEXT(
'Core Data for Automotive Mechanical Design Process');
#11868=PRODUCT_CONTEXT('part definition',#11867,'mechanical');
#11900=PRODUCT('Adjustment nut','Adjustment nut','Adjustment nut',(#11868));
#11968=COLOUR_RGB('Black',0.12,0.14,0.17);
#11969=FILL_AREA_STYLE_COLOUR('',#11968);
#11970=FILL_AREA_STYLE('',(#11969));
#11971=SURFACE_STYLE_FILL_AREA(#11970);
#11972=SURFACE_SIDE_STYLE('',(#11971));
#11973=SURFACE_STYLE_USAGE(.BOTH.,#11972);
#11974=PRESENTATION_STYLE_ASSIGNMENT((#11973));
ENDSEC;
END-ISO-10303-21;
